ISO-10303-21;
HEADER;
/* Generated by software containing ST-Developer
 * from STEP Tools, Inc. (www.steptools.com) 
 */

FILE_DESCRIPTION(
/* description */ ('PAT-080'),
/* implementation_level */ '2;1');

FILE_NAME(
/* name */ 'Bonded pad.step',
/* time_stamp */ '2026-10-29T20:13:47-07:00',
/* author */ (''),
/* organization */ (''),
/* preprocessor_version */ 'ST-DEVELOPER v20.2',
/* originating_system */ 'Autodesk Translation Framework v15.17.0.0',
/* authorisation */ '');

FILE_SCHEMA (('AUTOMOTIVE_DESIGN { 1 0 10303 214 3 1 1 }'));
ENDSEC;

DATA;
#10=MECHANICAL_DESIGN_GEOMETRIC_PRESENTATION_REPRESENTATION('',(#247),#6878);
#209=SHAPE_REPRESENTATION_RELATIONSHIP('SRR','None',#6965,#228);
#228=ADVANCED_BREP_SHAPE_REPRESENTATION('',(#266),#6860);
#247=STYLED_ITEM('',(#7143),#266);
#266=MANIFOLD_SOLID_BREP('Body1',#3863);
#363=PLANE('',#4115);
#364=PLANE('',#4116);
#365=PLANE('',#4117);
#366=PLANE('',#4118);
#367=PLANE('',#4119);
#368=PLANE('',#4120);
#510=FACE_OUTER_BOUND('',#744,.T.);
#511=FACE_OUTER_BOUND('',#745,.T.);
#512=FACE_OUTER_BOUND('',#746,.T.);
#513=FACE_OUTER_BOUND('',#747,.T.);
#514=FACE_OUTER_BOUND('',#748,.T.);
#515=FACE_OUTER_BOUND('',#749,.T.);
#744=EDGE_LOOP('',(#2656,#2657,#2658,#2659));
#745=EDGE_LOOP('',(#2660,#2661,#2662,#2663));
#746=EDGE_LOOP('',(#2664,#2665,#2666,#2667));
#747=EDGE_LOOP('',(#2668,#2669,#2670,#2671));
#748=EDGE_LOOP('',(#2672,#2673,#2674,#2675));
#749=EDGE_LOOP('',(#2676,#2677,#2678,#2679));
#1044=LINE('',#5785,#1359);
#1045=LINE('',#5787,#1360);
#1046=LINE('',#5789,#1361);
#1047=LINE('',#5790,#1362);
#1048=LINE('',#5793,#1363);
#1049=LINE('',#5795,#1364);
#1050=LINE('',#5796,#1365);
#1051=LINE('',#5799,#1366);
#1052=LINE('',#5801,#1367);
#1053=LINE('',#5802,#1368);
#1054=LINE('',#5804,#1369);
#1055=LINE('',#5805,#1370);
#1359=VECTOR('',#4594,1.);
#1360=VECTOR('',#4595,1.);
#1361=VECTOR('',#4596,1.);
#1362=VECTOR('',#4597,1.);
#1363=VECTOR('',#4600,1.);
#1364=VECTOR('',#4601,1.);
#1365=VECTOR('',#4602,1.);
#1366=VECTOR('',#4605,1.);
#1367=VECTOR('',#4606,1.);
#1368=VECTOR('',#4607,1.);
#1369=VECTOR('',#4610,1.);
#1370=VECTOR('',#4611,1.);
#1826=VERTEX_POINT('',#5783);
#1827=VERTEX_POINT('',#5784);
#1828=VERTEX_POINT('',#5786);
#1829=VERTEX_POINT('',#5788);
#1830=VERTEX_POINT('',#5792);
#1831=VERTEX_POINT('',#5794);
#1832=VERTEX_POINT('',#5798);
#1833=VERTEX_POINT('',#5800);
#2151=EDGE_CURVE('',#1826,#1827,#1044,.T.);
#2152=EDGE_CURVE('',#1827,#1828,#1045,.T.);
#2153=EDGE_CURVE('',#1829,#1828,#1046,.T.);
#2154=EDGE_CURVE('',#1826,#1829,#1047,.T.);
#2155=EDGE_CURVE('',#1830,#1826,#1048,.T.);
#2156=EDGE_CURVE('',#1831,#1829,#1049,.T.);
#2157=EDGE_CURVE('',#1830,#1831,#1050,.T.);
#2158=EDGE_CURVE('',#1832,#1830,#1051,.T.);
#2159=EDGE_CURVE('',#1833,#1831,#1052,.T.);
#2160=EDGE_CURVE('',#1832,#1833,#1053,.T.);
#2161=EDGE_CURVE('',#1827,#1832,#1054,.T.);
#2162=EDGE_CURVE('',#1828,#1833,#1055,.T.);
#2656=ORIENTED_EDGE('',*,*,#2151,.T.);
#2657=ORIENTED_EDGE('',*,*,#2152,.T.);
#2658=ORIENTED_EDGE('',*,*,#2153,.F.);
#2659=ORIENTED_EDGE('',*,*,#2154,.F.);
#2660=ORIENTED_EDGE('',*,*,#2155,.T.);
#2661=ORIENTED_EDGE('',*,*,#2154,.T.);
#2662=ORIENTED_EDGE('',*,*,#2156,.F.);
#2663=ORIENTED_EDGE('',*,*,#2157,.F.);
#2664=ORIENTED_EDGE('',*,*,#2158,.T.);
#2665=ORIENTED_EDGE('',*,*,#2157,.T.);
#2666=ORIENTED_EDGE('',*,*,#2159,.F.);
#2667=ORIENTED_EDGE('',*,*,#2160,.F.);
#2668=ORIENTED_EDGE('',*,*,#2161,.T.);
#2669=ORIENTED_EDGE('',*,*,#2160,.T.);
#2670=ORIENTED_EDGE('',*,*,#2162,.F.);
#2671=ORIENTED_EDGE('',*,*,#2152,.F.);
#2672=ORIENTED_EDGE('',*,*,#2162,.T.);
#2673=ORIENTED_EDGE('',*,*,#2159,.T.);
#2674=ORIENTED_EDGE('',*,*,#2156,.T.);
#2675=ORIENTED_EDGE('',*,*,#2153,.T.);
#2676=ORIENTED_EDGE('',*,*,#2161,.F.);
#2677=ORIENTED_EDGE('',*,*,#2151,.F.);
#2678=ORIENTED_EDGE('',*,*,#2155,.F.);
#2679=ORIENTED_EDGE('',*,*,#2158,.F.);
#3646=ADVANCED_FACE('',(#510),#363,.T.);
#3647=ADVANCED_FACE('',(#511),#364,.T.);
#3648=ADVANCED_FACE('',(#512),#365,.T.);
#3649=ADVANCED_FACE('',(#513),#366,.T.);
#3650=ADVANCED_FACE('',(#514),#367,.T.);
#3651=ADVANCED_FACE('',(#515),#368,.F.);
#3863=CLOSED_SHELL('',(#3646,#3647,#3648,#3649,#3650,#3651));
#4114=AXIS2_PLACEMENT_3D('',#5781,#4590,#4591);
#4115=AXIS2_PLACEMENT_3D('',#5782,#4592,#4593);
#4116=AXIS2_PLACEMENT_3D('',#5791,#4598,#4599);
#4117=AXIS2_PLACEMENT_3D('',#5797,#4603,#4604);
#4118=AXIS2_PLACEMENT_3D('',#5803,#4608,#4609);
#4119=AXIS2_PLACEMENT_3D('',#5806,#4612,#4613);
#4120=AXIS2_PLACEMENT_3D('',#5807,#4614,#4615);
#4590=DIRECTION('axis',(0.,0.,1.));
#4591=DIRECTION('refdir',(1.,0.,0.));
#4592=DIRECTION('center_axis',(0.,1.,0.));
#4593=DIRECTION('ref_axis',(-1.,0.,0.));
#4594=DIRECTION('',(-1.,0.,0.));
#4595=DIRECTION('',(0.,0.,1.));
#4596=DIRECTION('',(-1.,0.,0.));
#4597=DIRECTION('',(0.,0.,1.));
#4598=DIRECTION('center_axis',(1.,0.,0.));
#4599=DIRECTION('ref_axis',(0.,1.,0.));
#4600=DIRECTION('',(0.,1.,0.));
#4601=DIRECTION('',(0.,1.,0.));
#4602=DIRECTION('',(0.,0.,1.));
#4603=DIRECTION('center_axis',(0.,-1.,0.));
#4604=DIRECTION('ref_axis',(1.,0.,0.));
#4605=DIRECTION('',(1.,0.,0.));
#4606=DIRECTION('',(1.,0.,0.));
#4607=DIRECTION('',(0.,0.,1.));
#4608=DIRECTION('center_axis',(-1.,0.,0.));
#4609=DIRECTION('ref_axis',(0.,-1.,0.));
#4610=DIRECTION('',(0.,-1.,0.));
#4611=DIRECTION('',(0.,-1.,0.));
#4612=DIRECTION('center_axis',(0.,0.,1.));
#4613=DIRECTION('ref_axis',(1.,0.,0.));
#4614=DIRECTION('center_axis',(0.,0.,1.));
#4615=DIRECTION('ref_axis',(1.,0.,0.));
#5781=CARTESIAN_POINT('',(0.,0.,0.));
#5782=CARTESIAN_POINT('Origin',(-12.,5.,-0.3));
#5783=CARTESIAN_POINT('',(-12.,5.,-0.3));
#5784=CARTESIAN_POINT('',(-14.,5.,-0.3));
#5785=CARTESIAN_POINT('',(-12.,5.,-0.3));
#5786=CARTESIAN_POINT('',(-14.,5.,0.));
#5787=CARTESIAN_POINT('',(-14.,5.,-0.3));
#5788=CARTESIAN_POINT('',(-12.,5.,0.));
#5789=CARTESIAN_POINT('',(-12.,5.,0.));
#5790=CARTESIAN_POINT('',(-12.,5.,-0.3));
#5791=CARTESIAN_POINT('Origin',(-12.,-5.,-0.3));
#5792=CARTESIAN_POINT('',(-12.,-5.,-0.3));
#5793=CARTESIAN_POINT('',(-12.,-5.,-0.3));
#5794=CARTESIAN_POINT('',(-12.,-5.,0.));
#5795=CARTESIAN_POINT('',(-12.,-5.,0.));
#5796=CARTESIAN_POINT('',(-12.,-5.,-0.3));
#5797=CARTESIAN_POINT('Origin',(-14.,-5.,-0.3));
#5798=CARTESIAN_POINT('',(-14.,-5.,-0.3));
#5799=CARTESIAN_POINT('',(-14.,-5.,-0.3));
#5800=CARTESIAN_POINT('',(-14.,-5.,0.));
#5801=CARTESIAN_POINT('',(-14.,-5.,0.));
#5802=CARTESIAN_POINT('',(-14.,-5.,-0.3));
#5803=CARTESIAN_POINT('Origin',(-14.,5.,-0.3));
#5804=CARTESIAN_POINT('',(-14.,5.,-0.3));
#5805=CARTESIAN_POINT('',(-14.,5.,0.));
#5806=CARTESIAN_POINT('Origin',(-13.,0.,0.));
#5807=CARTESIAN_POINT('Origin',(-13.,0.,-0.3));
#6839=UNCERTAINTY_MEASURE_WITH_UNIT(LENGTH_MEASURE(0.001),#6879,
'DISTANCE_ACCURACY_VALUE',
'Maximum model space distance between geometric entities at asserted c
onnectivities');
#6857=UNCERTAINTY_MEASURE_WITH_UNIT(LENGTH_MEASURE(0.001),#6879,
'DISTANCE_ACCURACY_VALUE',
'Maximum model space distance between geometric entities at asserted c
onnectivities');
#6860=(
GEOMETRIC_REPRESENTATION_CONTEXT(3)
GLOBAL_UNCERTAINTY_ASSIGNED_CONTEXT((#6839))
GLOBAL_UNIT_ASSIGNED_CONTEXT((#6879,#6881,#6882))
REPRESENTATION_CONTEXT('','3D')
);
#6878=(
GEOMETRIC_REPRESENTATION_CONTEXT(3)
GLOBAL_UNCERTAINTY_ASSIGNED_CONTEXT((#6857))
GLOBAL_UNIT_ASSIGNED_CONTEXT((#6879,#6881,#6882))
REPRESENTATION_CONTEXT('','3D')
);
#6879=(
LENGTH_UNIT()
NAMED_UNIT(*)
SI_UNIT(.CENTI.,.METRE.)
);
#6881=(
NAMED_UNIT(*)
PLANE_ANGLE_UNIT()
SI_UNIT($,.RADIAN.)
);
#6882=(
NAMED_UNIT(*)
SI_UNIT($,.STERADIAN.)
SOLID_ANGLE_UNIT()
);
#6885=SHAPE_DEFINITION_REPRESENTATION(#6905,#6965);
#6905=PRODUCT_DEFINITION_SHAPE('',$,#6986);
#6965=SHAPE_REPRESENTATION('',(#4114),#6860);
#6983=PRODUCT_DEFINITION_CONTEXT('part definition',#7045,'design');
#6986=PRODUCT_DEFINITION('Bonded pad','Bonded pad',#7006,
#6983);
#7006=PRODUCT_DEFINITION_FORMATION('',$,#7049);
#7045=APPLICATION_CONTEXT(
'Core Data for Automotive Mechanical Design Process');
#7046=PRODUCT_CONTEXT('part definition',#7045,'mechanical');
#7049=PRODUCT('Bonded pad','Bonded pad','Bonded pad',(#7046));
#7137=COLOUR_RGB('Off White',0.89,0.88,0.83);
#7138=FILL_AREA_STYLE_COLOUR('',#7137);
#7139=FILL_AREA_STYLE('',(#7138));
#7140=SURFACE_STYLE_FILL_AREA(#7139);
#7141=SURFACE_SIDE_STYLE('',(#7140));
#7142=SURFACE_STYLE_USAGE(.BOTH.,#7141);
#7143=PRESENTATION_STYLE_ASSIGNMENT((#7142));
ENDSEC;
END-ISO-10303-21;
